ISO-10303-21;
HEADER;
FILE_DESCRIPTION (('STEP AP214'),
    '1' );
FILE_NAME ('Link.step',
    '2026-10-23T20:35:44',
    ( '' ),
    ( '' ),
    'SwSTEP 2.0',
    'SolidWorks 2025',
    '' );
FILE_SCHEMA (( 'AUTOMOTIVE_DESIGN' ));
ENDSEC;

DATA;
#18=VERTEX_POINT ( 'NONE', #5013 ) ;
#22=CIRCLE ( 'NONE', #2939, 0.4921259842519685179 ) ;
#61=CARTESIAN_POINT ( 'NONE',  ( 2.892866454678787531E-17, 0.000000000000000000, 0.2362204724409449341 ) ) ;
#63=PRODUCT_DEFINITION_CONTEXT ( 'detailed design', #3952, 'design' ) ;
#79=DIRECTION ( 'NONE',  ( -1.000000000000000000, -0.000000000000000000, -0.000000000000000000 ) ) ;
#84=CYLINDRICAL_SURFACE ( 'NONE', #4175, 0.2362204724409449341 ) ;
#91=LINE ( 'NONE', #2420, #7062 ) ;
#95=EDGE_CURVE ( 'NONE', #3796, #3264, #4939, .T. ) ;
#127=ORIENTED_EDGE ( 'NONE', *, *, #95, .F. ) ;
#138=CARTESIAN_POINT ( 'NONE',  ( 0.000000000000000000, 0.000000000000000000, 0.000000000000000000 ) ) ;
#145=EDGE_CURVE ( 'NONE', #322, #18, #7008, .T. ) ;
#223=VECTOR ( 'NONE', #79, 39.37007874015748143 ) ;
#242=ORIENTED_EDGE ( 'NONE', *, *, #1147, .F. ) ;
#306=CYLINDRICAL_SURFACE ( 'NONE', #3807, 0.2362204724409455170 ) ;
#322=VERTEX_POINT ( 'NONE', #3083 ) ;
#335=FACE_OUTER_BOUND ( 'NONE', #5189, .T. ) ;
#402=ORIENTED_EDGE ( 'NONE', *, *, #6794, .T. ) ;
#418=CARTESIAN_POINT ( 'NONE',  ( 0.000000000000000000, 0.000000000000000000, 0.000000000000000000 ) ) ;
#448=VERTEX_POINT ( 'NONE', #6828 ) ;
#453=CARTESIAN_POINT ( 'NONE',  ( 0.000000000000000000, 0.2559055118110236116, 0.000000000000000000 ) ) ;
#544=DIRECTION ( 'NONE',  ( 0.000000000000000000, 1.000000000000000000, 0.000000000000000000 ) ) ;
#566=DIRECTION ( 'NONE',  ( 0.000000000000000000, 0.000000000000000000, 1.000000000000000000 ) ) ;
#661=EDGE_CURVE ( 'NONE', #4786, #3796, #1755, .T. ) ;
#706=EDGE_CURVE ( 'NONE', #2864, #1140, #22, .T. ) ;
#707=CARTESIAN_POINT ( 'NONE',  ( 0.000000000000000000, 0.2559055118110236116, -0.2362204724409449341 ) ) ;
#741=ORIENTED_EDGE ( 'NONE', *, *, #3231, .F. ) ;
#751=ADVANCED_FACE ( 'NONE', ( #1841 ), #84, .F. ) ;
#766=VECTOR ( 'NONE', #2837, 39.37007874015748143 ) ;
#777=PRODUCT_CONTEXT ( 'NONE', #915, 'mechanical' ) ;
#797=FACE_OUTER_BOUND ( 'NONE', #6325, .T. ) ;
#817=LINE ( 'NONE', #7304, #1421 ) ;
#861=AXIS2_PLACEMENT_3D ( 'NONE', #4913, #7238, #6321 ) ;
#866=DIRECTION ( 'NONE',  ( -0.000000000000000000, -1.000000000000000000, -0.000000000000000000 ) ) ;
#871=DIRECTION ( 'NONE',  ( -0.000000000000000000, -1.000000000000000000, -0.000000000000000000 ) ) ;
#880=CARTESIAN_POINT ( 'NONE',  ( 7.874015748031496287, 0.000000000000000000, 0.000000000000000000 ) ) ;
#904=CYLINDRICAL_SURFACE ( 'NONE', #5507, 0.4921259842519685179 ) ;
#915=APPLICATION_CONTEXT ( 'automotive_design' ) ;
#997=VERTEX_POINT ( 'NONE', #6319 ) ;
#1006=DIRECTION ( 'NONE',  ( 0.000000000000000000, 1.000000000000000000, 0.000000000000000000 ) ) ;
#1008=LINE ( 'NONE', #2236, #766 ) ;
#1018=EDGE_CURVE ( 'NONE', #5096, #997, #4629, .T. ) ;
#1045=VERTEX_POINT ( 'NONE', #4169 ) ;
#1064=ORIENTED_EDGE ( 'NONE', *, *, #2383, .F. ) ;
#1096=CARTESIAN_POINT ( 'NONE',  ( 0.000000000000000000, 0.000000000000000000, 0.000000000000000000 ) ) ;
#1140=VERTEX_POINT ( 'NONE', #2478 ) ;
#1143=CARTESIAN_POINT ( 'NONE',  ( 7.874015748031496287, 0.000000000000000000, -0.2362204724409455170 ) ) ;
#1147=EDGE_CURVE ( 'NONE', #3264, #3796, #6256, .T. ) ;
#1195=AXIS2_PLACEMENT_3D ( 'NONE', #1895, #3110, #7240 ) ;
#1210=LINE ( 'NONE', #5977, #223 ) ;
#1276=CARTESIAN_POINT ( 'NONE',  ( 0.000000000000000000, 0.000000000000000000, -0.4921259842519685179 ) ) ;
#1281=LINE ( 'NONE', #1908, #5738 ) ;
#1307=SHAPE_REPRESENTATION ( 'Link', ( #5166 ), #4787 ) ;
#1328=VECTOR ( 'NONE', #1791, 39.37007874015748143 ) ;
#1356=UNCERTAINTY_MEASURE_WITH_UNIT (LENGTH_MEASURE( 1.000000000000000082E-05 ), #1698, 'distance_accuracy_value', 'NONE');
#1360=DIRECTION ( 'NONE',  ( -0.000000000000000000, -1.000000000000000000, -0.000000000000000000 ) ) ;
#1396=PLANE ( 'NONE',  #1949 ) ;
#1421=VECTOR ( 'NONE', #2082, 39.37007874015748143 ) ;
#1430=DIRECTION ( 'NONE',  ( 0.000000000000000000, 0.000000000000000000, -1.000000000000000000 ) ) ;
#1454=ORIENTED_EDGE ( 'NONE', *, *, #6089, .T. ) ;
#1499=ORIENTED_EDGE ( 'NONE', *, *, #1018, .T. ) ;
#1511=ORIENTED_EDGE ( 'NONE', *, *, #2020, .T. ) ;
#1549=CARTESIAN_POINT ( 'NONE',  ( 7.874015748031496287, 0.2559055118110236116, -0.2362204724409455170 ) ) ;
#1572=DIRECTION ( 'NONE',  ( 0.000000000000000000, -0.000000000000000000, 1.000000000000000000 ) ) ;
#1684=DIRECTION ( 'NONE',  ( -1.000000000000000000, -0.000000000000000000, -0.000000000000000000 ) ) ;
#1698=( CONVERSION_BASED_UNIT ( 'INCH', #2914 ) LENGTH_UNIT ( ) NAMED_UNIT ( #7497 ) );
#1736=DIRECTION ( 'NONE',  ( 0.000000000000000000, 0.000000000000000000, 1.000000000000000000 ) ) ;
#1737=CYLINDRICAL_SURFACE ( 'NONE', #6153, 0.2362204724409449341 ) ;
#1755=LINE ( 'NONE', #2241, #3814 ) ;
#1782=ORIENTED_EDGE ( 'NONE', *, *, #2292, .F. ) ;
#1791=DIRECTION ( 'NONE',  ( 1.000000000000000000, 0.000000000000000000, 0.000000000000000000 ) ) ;
#1805=SHAPE_REPRESENTATION_RELATIONSHIP ( 'NONE' , 'NONE' ,  #1307, #6511 ) ;
#1814=ADVANCED_FACE ( 'NONE', ( #7065, #3378, #4526 ), #6930, .T. ) ;
#1841=FACE_OUTER_BOUND ( 'NONE', #4334, .T. ) ;
#1847=LINE ( 'NONE', #707, #3775 ) ;
#1874=DIRECTION ( 'NONE',  ( 0.000000000000000000, 1.000000000000000000, 0.000000000000000000 ) ) ;
#1885=ORIENTED_EDGE ( 'NONE', *, *, #2117, .F. ) ;
#1895=CARTESIAN_POINT ( 'NONE',  ( 0.000000000000000000, 0.2559055118110236116, 0.4921259842519685179 ) ) ;
#1908=CARTESIAN_POINT ( 'NONE',  ( 0.000000000000000000, 0.2559055118110236116, 0.4921259842519685179 ) ) ;
#1923=EDGE_LOOP ( 'NONE', ( #1885, #6288, #3217, #242 ) ) ;
#1946=EDGE_LOOP ( 'NONE', ( #5786, #3725, #7037, #2047 ) ) ;
#1949=AXIS2_PLACEMENT_3D ( 'NONE', #4237, #3164, #3667 ) ;
#1984=DIRECTION ( 'NONE',  ( 0.000000000000000000, 1.000000000000000000, 0.000000000000000000 ) ) ;
#1999=ORIENTED_EDGE ( 'NONE', *, *, #5233, .F. ) ;
#2020=EDGE_CURVE ( 'NONE', #1140, #1045, #6049, .T. ) ;
#2047=ORIENTED_EDGE ( 'NONE', *, *, #4027, .T. ) ;
#2082=DIRECTION ( 'NONE',  ( -0.000000000000000000, -1.000000000000000000, -0.000000000000000000 ) ) ;
#2101=VECTOR ( 'NONE', #1684, 39.37007874015748143 ) ;
#2117=EDGE_CURVE ( 'NONE', #2154, #3264, #6573, .T. ) ;
#2134=DIRECTION ( 'NONE',  ( 0.000000000000000000, 0.000000000000000000, 1.000000000000000000 ) ) ;
#2154=VERTEX_POINT ( 'NONE', #3045 ) ;
#2161=EDGE_CURVE ( 'NONE', #1045, #7070, #2787, .T. ) ;
#2175=AXIS2_PLACEMENT_3D ( 'NONE', #2590, #871, #1430 ) ;
#2231=AXIS2_PLACEMENT_3D ( 'NONE', #5196, #4006, #1736 ) ;
#2236=CARTESIAN_POINT ( 'NONE',  ( 2.892866454678787531E-17, 0.2559055118110236116, 0.2362204724409449341 ) ) ;
#2239=DIMENSIONAL_EXPONENTS ( 1.000000000000000000, 0.000000000000000000, 0.000000000000000000, 0.000000000000000000, 0.000000000000000000, 0.000000000000000000, 0.000000000000000000 ) ;
#2241=CARTESIAN_POINT ( 'NONE',  ( 7.874015748031496287, 0.2559055118110236116, -0.2362204724409455170 ) ) ;
#2254=AXIS2_PLACEMENT_3D ( 'NONE', #6692, #4974, #6726 ) ;
#2269=ORIENTED_EDGE ( 'NONE', *, *, #145, .T. ) ;
#2292=EDGE_CURVE ( 'NONE', #5027, #448, #4384, .T. ) ;
#2307=FACE_OUTER_BOUND ( 'NONE', #5911, .T. ) ;
#2316=AXIS2_PLACEMENT_3D ( 'NONE', #6416, #1874, #4695 ) ;
#2318=ORIENTED_EDGE ( 'NONE', *, *, #6794, .F. ) ;
#2369=LINE ( 'NONE', #6467, #1328 ) ;
#2380=VERTEX_POINT ( 'NONE', #5005 ) ;
#2383=EDGE_CURVE ( 'NONE', #4290, #1140, #1281, .T. ) ;
#2420=CARTESIAN_POINT ( 'NONE',  ( 7.874015748031496287, 0.2559055118110236116, 0.4921259842519685179 ) ) ;
#2425=( NAMED_UNIT ( * ) SI_UNIT ( $, .STERADIAN. ) SOLID_ANGLE_UNIT ( ) );
#2460=DIRECTION ( 'NONE',  ( -0.000000000000000000, -1.000000000000000000, -0.000000000000000000 ) ) ;
#2466=DIRECTION ( 'NONE',  ( 0.000000000000000000, 0.000000000000000000, 1.000000000000000000 ) ) ;
#2478=CARTESIAN_POINT ( 'NONE',  ( 0.000000000000000000, 0.000000000000000000, 0.4921259842519685179 ) ) ;
#2489=DIRECTION ( 'NONE',  ( 0.000000000000000000, 0.000000000000000000, 1.000000000000000000 ) ) ;
#2527=ORIENTED_EDGE ( 'NONE', *, *, #2712, .T. ) ;
#2567=DIRECTION ( 'NONE',  ( -0.000000000000000000, -1.000000000000000000, -0.000000000000000000 ) ) ;
#2590=CARTESIAN_POINT ( 'NONE',  ( 7.874015748031496287, 0.2559055118110236116, 0.000000000000000000 ) ) ;
#2676=LINE ( 'NONE', #6062, #7473 ) ;
#2677=ORIENTED_EDGE ( 'NONE', *, *, #145, .F. ) ;
#2681=CIRCLE ( 'NONE', #3175, 0.2362204724409449341 ) ;
#2689=( NAMED_UNIT ( * ) SI_UNIT ( $, .STERADIAN. ) SOLID_ANGLE_UNIT ( ) );
#2712=EDGE_CURVE ( 'NONE', #2380, #1045, #91, .T. ) ;
#2715=EDGE_CURVE ( 'NONE', #18, #448, #1847, .T. ) ;
#2741=DIRECTION ( 'NONE',  ( 1.000000000000000000, 0.000000000000000000, 0.000000000000000000 ) ) ;
#2745=PRODUCT_DEFINITION ( 'UNKNOWN', '', #3750, #63 ) ;
#2787=CIRCLE ( 'NONE', #3771, 0.4921259842519685179 ) ;
#2837=DIRECTION ( 'NONE',  ( -0.000000000000000000, -1.000000000000000000, -0.000000000000000000 ) ) ;
#2864=VERTEX_POINT ( 'NONE', #1276 ) ;
#2914=LENGTH_MEASURE_WITH_UNIT ( LENGTH_MEASURE( 0.02539999999999999897 ), #5804 );
#2939=AXIS2_PLACEMENT_3D ( 'NONE', #4868, #3686, #4903 ) ;
#2957=DIRECTION ( 'NONE',  ( 0.000000000000000000, 1.000000000000000000, 0.000000000000000000 ) ) ;
#2966=DIRECTION ( 'NONE',  ( 0.000000000000000000, 0.000000000000000000, 1.000000000000000000 ) ) ;
#3023=ADVANCED_FACE ( 'NONE', ( #2307 ), #3611, .F. ) ;
#3045=CARTESIAN_POINT ( 'NONE',  ( 7.874015748031496287, 0.2559055118110236116, 0.2362204724409455170 ) ) ;
#3079=ADVANCED_FACE ( 'NONE', ( #3624 ), #1396, .F. ) ;
#3083=CARTESIAN_POINT ( 'NONE',  ( 2.892866454678787531E-17, 0.2559055118110236116, 0.2362204724409449341 ) ) ;
#3091=CARTESIAN_POINT ( 'NONE',  ( 0.000000000000000000, 0.000000000000000000, 0.4921259842519685179 ) ) ;
#3093=ORIENTED_EDGE ( 'NONE', *, *, #4961, .T. ) ;
#3110=DIRECTION ( 'NONE',  ( 0.000000000000000000, 0.000000000000000000, -1.000000000000000000 ) ) ;
#3164=DIRECTION ( 'NONE',  ( 0.000000000000000000, 0.000000000000000000, 1.000000000000000000 ) ) ;
#3175=AXIS2_PLACEMENT_3D ( 'NONE', #138, #4300, #6566 ) ;
#3195=PRODUCT_DEFINITION_SHAPE ( 'NONE', 'NONE',  #2745 ) ;
#3201=DIRECTION ( 'NONE',  ( 0.000000000000000000, 0.000000000000000000, -1.000000000000000000 ) ) ;
#3210=CARTESIAN_POINT ( 'NONE',  ( 7.874015748031496287, 0.000000000000000000, -0.4921259842519685179 ) ) ;
#3216=EDGE_LOOP ( 'NONE', ( #5206, #7195, #6820, #4849 ) ) ;
#3217=ORIENTED_EDGE ( 'NONE', *, *, #661, .T. ) ;
#3227=CLOSED_SHELL ( 'NONE', ( #7427, #751, #1814, #6827, #3361, #3023, #4755, #3079, #6141, #4917 ) ) ;
#3228=( CONVERSION_BASED_UNIT ( 'INCH', #7310 ) LENGTH_UNIT ( ) NAMED_UNIT ( #2239 ) );
#3231=EDGE_CURVE ( 'NONE', #4290, #2380, #2369, .T. ) ;
#3249=DIRECTION ( 'NONE',  ( -0.000000000000000000, -1.000000000000000000, -0.000000000000000000 ) ) ;
#3264=VERTEX_POINT ( 'NONE', #3878 ) ;
#3269=DIRECTION ( 'NONE',  ( 0.000000000000000000, 0.000000000000000000, 1.000000000000000000 ) ) ;
#3287=ORIENTED_EDGE ( 'NONE', *, *, #3427, .F. ) ;
#3306=AXIS2_PLACEMENT_3D ( 'NONE', #5851, #5273, #2489 ) ;
#3361=ADVANCED_FACE ( 'NONE', ( #335 ), #904, .T. ) ;
#3378=FACE_OUTER_BOUND ( 'NONE', #3861, .T. ) ;
#3427=EDGE_CURVE ( 'NONE', #448, #5027, #2681, .T. ) ;
#3462=AXIS2_PLACEMENT_3D ( 'NONE', #7317, #5043, #3269 ) ;
#3501=EDGE_CURVE ( 'NONE', #18, #322, #5748, .T. ) ;
#3512=FACE_BOUND ( 'NONE', #4559, .T. ) ;
#3557=CARTESIAN_POINT ( 'NONE',  ( 0.000000000000000000, 0.2559055118110236116, 0.4921259842519685179 ) ) ;
#3574=ORIENTED_EDGE ( 'NONE', *, *, #4961, .F. ) ;
#3611=PLANE ( 'NONE',  #1195 ) ;
#3613=( NAMED_UNIT ( * ) PLANE_ANGLE_UNIT ( ) SI_UNIT ( $, .RADIAN. ) );
#3624=FACE_OUTER_BOUND ( 'NONE', #1946, .T. ) ;
#3667=DIRECTION ( 'NONE',  ( 1.000000000000000000, 0.000000000000000000, -0.000000000000000000 ) ) ;
#3686=DIRECTION ( 'NONE',  ( 0.000000000000000000, 1.000000000000000000, 0.000000000000000000 ) ) ;
#3719=AXIS2_PLACEMENT_3D ( 'NONE', #880, #6660, #3862 ) ;
#3725=ORIENTED_EDGE ( 'NONE', *, *, #5490, .F. ) ;
#3738=FACE_OUTER_BOUND ( 'NONE', #5646, .T. ) ;
#3750=PRODUCT_DEFINITION_FORMATION_WITH_SPECIFIED_SOURCE ( 'ANY', '', #5591, .NOT_KNOWN. ) ;
#3768=ORIENTED_EDGE ( 'NONE', *, *, #2715, .T. ) ;
#3771=AXIS2_PLACEMENT_3D ( 'NONE', #4886, #1984, #2966 ) ;
#3775=VECTOR ( 'NONE', #2460, 39.37007874015748143 ) ;
#3796=VERTEX_POINT ( 'NONE', #1143 ) ;
#3807=AXIS2_PLACEMENT_3D ( 'NONE', #6078, #5430, #3201 ) ;
#3811=AXIS2_PLACEMENT_3D ( 'NONE', #5921, #5839, #566 ) ;
#3814=VECTOR ( 'NONE', #4571, 39.37007874015748143 ) ;
#3861=EDGE_LOOP ( 'NONE', ( #402, #5537, #3093, #1499 ) ) ;
#3862=DIRECTION ( 'NONE',  ( 0.000000000000000000, 0.000000000000000000, 1.000000000000000000 ) ) ;
#3866=DIRECTION ( 'NONE',  ( 0.000000000000000000, 0.000000000000000000, 1.000000000000000000 ) ) ;
#3878=CARTESIAN_POINT ( 'NONE',  ( 7.874015748031496287, 0.000000000000000000, 0.2362204724409455170 ) ) ;
#3936=FACE_OUTER_BOUND ( 'NONE', #1923, .T. ) ;
#3952=APPLICATION_CONTEXT ( 'automotive_design' ) ;
#3990=ORIENTED_EDGE ( 'NONE', *, *, #95, .T. ) ;
#4006=DIRECTION ( 'NONE',  ( 0.000000000000000000, 1.000000000000000000, 0.000000000000000000 ) ) ;
#4027=EDGE_CURVE ( 'NONE', #5096, #7070, #817, .T. ) ;
#4079=CARTESIAN_POINT ( 'NONE',  ( 0.000000000000000000, 0.2559055118110236116, 0.000000000000000000 ) ) ;
#4084=ORIENTED_EDGE ( 'NONE', *, *, #4027, .F. ) ;
#4125=ORIENTED_EDGE ( 'NONE', *, *, #5490, .T. ) ;
#4128=ORIENTED_EDGE ( 'NONE', *, *, #3501, .T. ) ;
#4157=CIRCLE ( 'NONE', #3306, 0.4921259842519685179 ) ;
#4169=CARTESIAN_POINT ( 'NONE',  ( 7.874015748031496287, 0.000000000000000000, 0.4921259842519685179 ) ) ;
#4175=AXIS2_PLACEMENT_3D ( 'NONE', #4220, #2567, #5363 ) ;
#4220=CARTESIAN_POINT ( 'NONE',  ( 0.000000000000000000, 0.2559055118110236116, 0.000000000000000000 ) ) ;
#4237=CARTESIAN_POINT ( 'NONE',  ( 0.000000000000000000, 0.2559055118110236116, -0.4921259842519685179 ) ) ;
#4243=FACE_BOUND ( 'NONE', #5854, .T. ) ;
#4248=ORIENTED_EDGE ( 'NONE', *, *, #5233, .T. ) ;
#4259=EDGE_CURVE ( 'NONE', #7070, #2864, #1210, .T. ) ;
#4290=VERTEX_POINT ( 'NONE', #3557 ) ;
#4295=ORIENTED_EDGE ( 'NONE', *, *, #2715, .F. ) ;
#4300=DIRECTION ( 'NONE',  ( 0.000000000000000000, 1.000000000000000000, 0.000000000000000000 ) ) ;
#4311=DIRECTION ( 'NONE',  ( 0.000000000000000000, 0.000000000000000000, -1.000000000000000000 ) ) ;
#4322=ORIENTED_EDGE ( 'NONE', *, *, #2161, .T. ) ;
#4334=EDGE_LOOP ( 'NONE', ( #4128, #4248, #3287, #4295 ) ) ;
#4343=EDGE_LOOP ( 'NONE', ( #1999, #2269, #3768, #1782 ) ) ;
#4359=ORIENTED_EDGE ( 'NONE', *, *, #661, .F. ) ;
#4381=DIRECTION ( 'NONE',  ( 0.000000000000000000, 0.000000000000000000, -1.000000000000000000 ) ) ;
#4384=CIRCLE ( 'NONE', #5238, 0.2362204724409449341 ) ;
#4414=( LENGTH_UNIT ( ) NAMED_UNIT ( * ) SI_UNIT ( $, .METRE. ) );
#4526=FACE_BOUND ( 'NONE', #6675, .T. ) ;
#4533=MECHANICAL_DESIGN_GEOMETRIC_PRESENTATION_REPRESENTATION('',(#6851),#5028);
#4559=EDGE_LOOP ( 'NONE', ( #5574, #6712 ) ) ;
#4571=DIRECTION ( 'NONE',  ( -0.000000000000000000, -1.000000000000000000, -0.000000000000000000 ) ) ;
#4629=LINE ( 'NONE', #6351, #2101 ) ;
#4695=DIRECTION ( 'NONE',  ( 0.000000000000000000, -0.000000000000000000, 1.000000000000000000 ) ) ;
#4708=UNCERTAINTY_MEASURE_WITH_UNIT (LENGTH_MEASURE( 1.000000000000000082E-05 ), #3228, 'distance_accuracy_value', 'NONE');
#4736=PLANE ( 'NONE',  #2316 ) ;
#4738=AXIS2_PLACEMENT_3D ( 'NONE', #6356, #1006, #1572 ) ;
#4755=ADVANCED_FACE ( 'NONE', ( #797 ), #5511, .T. ) ;
#4786=VERTEX_POINT ( 'NONE', #1549 ) ;
#4787=( GEOMETRIC_REPRESENTATION_CONTEXT ( 3 ) GLOBAL_UNCERTAINTY_ASSIGNED_CONTEXT ( ( #1356 ) ) GLOBAL_UNIT_ASSIGNED_CONTEXT ( ( #1698, #3613, #2425 ) ) REPRESENTATION_CONTEXT ( 'NONE', 'WORKASPACE' ) );
#4799=ORIENTED_EDGE ( 'NONE', *, *, #3501, .F. ) ;
#4849=ORIENTED_EDGE ( 'NONE', *, *, #2020, .F. ) ;
#4868=CARTESIAN_POINT ( 'NONE',  ( 0.000000000000000000, 0.000000000000000000, 0.000000000000000000 ) ) ;
#4886=CARTESIAN_POINT ( 'NONE',  ( 7.874015748031496287, 0.000000000000000000, 0.000000000000000000 ) ) ;
#4903=DIRECTION ( 'NONE',  ( 0.000000000000000000, 0.000000000000000000, 1.000000000000000000 ) ) ;
#4913=CARTESIAN_POINT ( 'NONE',  ( 0.000000000000000000, 0.2559055118110236116, 0.000000000000000000 ) ) ;
#4917=ADVANCED_FACE ( 'NONE', ( #3936 ), #6267, .F. ) ;
#4939=CIRCLE ( 'NONE', #3719, 0.2362204724409455170 ) ;
#4961=EDGE_CURVE ( 'NONE', #2380, #5096, #6505, .T. ) ;
#4974=DIRECTION ( 'NONE',  ( 0.000000000000000000, 1.000000000000000000, 0.000000000000000000 ) ) ;
#5005=CARTESIAN_POINT ( 'NONE',  ( 7.874015748031496287, 0.2559055118110236116, 0.4921259842519685179 ) ) ;
#5013=CARTESIAN_POINT ( 'NONE',  ( 0.000000000000000000, 0.2559055118110236116, -0.2362204724409449341 ) ) ;
#5027=VERTEX_POINT ( 'NONE', #61 ) ;
#5028=( GEOMETRIC_REPRESENTATION_CONTEXT ( 3 ) GLOBAL_UNCERTAINTY_ASSIGNED_CONTEXT ( ( #4708 ) ) GLOBAL_UNIT_ASSIGNED_CONTEXT ( ( #3228, #7351, #2689 ) ) REPRESENTATION_CONTEXT ( 'NONE', 'WORKASPACE' ) );
#5038=AXIS2_PLACEMENT_3D ( 'NONE', #6441, #2957, #2466 ) ;
#5039=DIRECTION ( 'NONE',  ( -0.000000000000000000, -1.000000000000000000, -0.000000000000000000 ) ) ;
#5043=DIRECTION ( 'NONE',  ( 0.000000000000000000, 1.000000000000000000, 0.000000000000000000 ) ) ;
#5096=VERTEX_POINT ( 'NONE', #5610 ) ;
#5125=DIRECTION ( 'NONE',  ( -0.000000000000000000, -1.000000000000000000, -0.000000000000000000 ) ) ;
#5138=ORIENTED_EDGE ( 'NONE', *, *, #1147, .T. ) ;
#5166=AXIS2_PLACEMENT_3D ( 'NONE', #418, #2134, #2741 ) ;
#5189=EDGE_LOOP ( 'NONE', ( #6056, #1064, #2318, #4125 ) ) ;
#5196=CARTESIAN_POINT ( 'NONE',  ( 7.874015748031496287, 0.2559055118110236116, 0.000000000000000000 ) ) ;
#5206=ORIENTED_EDGE ( 'NONE', *, *, #706, .F. ) ;
#5233=EDGE_CURVE ( 'NONE', #322, #5027, #1008, .T. ) ;
#5238=AXIS2_PLACEMENT_3D ( 'NONE', #1096, #544, #3866 ) ;
#5273=DIRECTION ( 'NONE',  ( 0.000000000000000000, 1.000000000000000000, 0.000000000000000000 ) ) ;
#5363=DIRECTION ( 'NONE',  ( 0.000000000000000000, 0.000000000000000000, -1.000000000000000000 ) ) ;
#5430=DIRECTION ( 'NONE',  ( -0.000000000000000000, -1.000000000000000000, -0.000000000000000000 ) ) ;
#5436=DIRECTION ( 'NONE',  ( -0.000000000000000000, -1.000000000000000000, -0.000000000000000000 ) ) ;
#5458=EDGE_LOOP ( 'NONE', ( #4799, #2677 ) ) ;
#5468=CARTESIAN_POINT ( 'NONE',  ( 7.874015748031496287, 0.2559055118110236116, 0.2362204724409455170 ) ) ;
#5490=EDGE_CURVE ( 'NONE', #997, #2864, #2676, .T. ) ;
#5493=VECTOR ( 'NONE', #1360, 39.37007874015748143 ) ;
#5507=AXIS2_PLACEMENT_3D ( 'NONE', #453, #5039, #4381 ) ;
#5511=CYLINDRICAL_SURFACE ( 'NONE', #2175, 0.4921259842519685179 ) ;
#5529=ORIENTED_EDGE ( 'NONE', *, *, #6316, .F. ) ;
#5537=ORIENTED_EDGE ( 'NONE', *, *, #3231, .T. ) ;
#5556=ORIENTED_EDGE ( 'NONE', *, *, #6089, .F. ) ;
#5574=ORIENTED_EDGE ( 'NONE', *, *, #3427, .T. ) ;
#5591=PRODUCT ( 'Link', 'Link', '', ( #777 ) ) ;
#5610=CARTESIAN_POINT ( 'NONE',  ( 7.874015748031496287, 0.2559055118110236116, -0.4921259842519685179 ) ) ;
#5616=VECTOR ( 'NONE', #5970, 39.37007874015748143 ) ;
#5646=EDGE_LOOP ( 'NONE', ( #1454, #6350, #127, #4359 ) ) ;
#5705=CARTESIAN_POINT ( 'NONE',  ( 7.874015748031496287, 0.2559055118110236116, 0.000000000000000000 ) ) ;
#5738=VECTOR ( 'NONE', #5436, 39.37007874015748143 ) ;
#5748=CIRCLE ( 'NONE', #861, 0.2362204724409449341 ) ;
#5786=ORIENTED_EDGE ( 'NONE', *, *, #4259, .T. ) ;
#5804=( LENGTH_UNIT ( ) NAMED_UNIT ( * ) SI_UNIT ( $, .METRE. ) );
#5837=DIRECTION ( 'NONE',  ( 0.000000000000000000, 0.000000000000000000, -1.000000000000000000 ) ) ;
#5839=DIRECTION ( 'NONE',  ( 0.000000000000000000, 1.000000000000000000, 0.000000000000000000 ) ) ;
#5851=CARTESIAN_POINT ( 'NONE',  ( 0.000000000000000000, 0.2559055118110236116, 0.000000000000000000 ) ) ;
#5854=EDGE_LOOP ( 'NONE', ( #3990, #5138 ) ) ;
#5870=ORIENTED_EDGE ( 'NONE', *, *, #2383, .T. ) ;
#5890=AXIS2_PLACEMENT_3D ( 'NONE', #5705, #5125, #5837 ) ;
#5911=EDGE_LOOP ( 'NONE', ( #1511, #7334, #741, #5870 ) ) ;
#5921=CARTESIAN_POINT ( 'NONE',  ( 7.874015748031496287, 0.2559055118110236116, 0.000000000000000000 ) ) ;
#5970=DIRECTION ( 'NONE',  ( 1.000000000000000000, 0.000000000000000000, 0.000000000000000000 ) ) ;
#5977=CARTESIAN_POINT ( 'NONE',  ( 0.000000000000000000, 0.000000000000000000, -0.4921259842519685179 ) ) ;
#6049=LINE ( 'NONE', #3091, #5616 ) ;
#6056=ORIENTED_EDGE ( 'NONE', *, *, #706, .T. ) ;
#6062=CARTESIAN_POINT ( 'NONE',  ( 0.000000000000000000, 0.2559055118110236116, -0.4921259842519685179 ) ) ;
#6078=CARTESIAN_POINT ( 'NONE',  ( 7.874015748031496287, 0.2559055118110236116, 0.000000000000000000 ) ) ;
#6089=EDGE_CURVE ( 'NONE', #4786, #2154, #7099, .T. ) ;
#6141=ADVANCED_FACE ( 'NONE', ( #6984 ), #1737, .F. ) ;
#6153=AXIS2_PLACEMENT_3D ( 'NONE', #4079, #866, #4311 ) ;
#6256=CIRCLE ( 'NONE', #5038, 0.2362204724409455170 ) ;
#6267=CYLINDRICAL_SURFACE ( 'NONE', #5890, 0.2362204724409455170 ) ;
#6288=ORIENTED_EDGE ( 'NONE', *, *, #6316, .T. ) ;
#6316=EDGE_CURVE ( 'NONE', #2154, #4786, #6493, .T. ) ;
#6319=CARTESIAN_POINT ( 'NONE',  ( 0.000000000000000000, 0.2559055118110236116, -0.4921259842519685179 ) ) ;
#6321=DIRECTION ( 'NONE',  ( 0.000000000000000000, 0.000000000000000000, 1.000000000000000000 ) ) ;
#6325=EDGE_LOOP ( 'NONE', ( #4322, #4084, #3574, #2527 ) ) ;
#6350=ORIENTED_EDGE ( 'NONE', *, *, #2117, .T. ) ;
#6351=CARTESIAN_POINT ( 'NONE',  ( 0.000000000000000000, 0.2559055118110236116, -0.4921259842519685179 ) ) ;
#6356=CARTESIAN_POINT ( 'NONE',  ( 0.000000000000000000, 0.2559055118110236116, 0.000000000000000000 ) ) ;
#6416=CARTESIAN_POINT ( 'NONE',  ( 0.000000000000000000, 0.000000000000000000, 0.000000000000000000 ) ) ;
#6441=CARTESIAN_POINT ( 'NONE',  ( 7.874015748031496287, 0.000000000000000000, 0.000000000000000000 ) ) ;
#6467=CARTESIAN_POINT ( 'NONE',  ( 0.000000000000000000, 0.2559055118110236116, 0.4921259842519685179 ) ) ;
#6493=CIRCLE ( 'NONE', #3462, 0.2362204724409455170 ) ;
#6505=CIRCLE ( 'NONE', #2231, 0.4921259842519685179 ) ;
#6511=ADVANCED_BREP_SHAPE_REPRESENTATION ( '', ( #6665, #5166 ), #4787 ) ;
#6566=DIRECTION ( 'NONE',  ( 0.000000000000000000, 0.000000000000000000, 1.000000000000000000 ) ) ;
#6573=LINE ( 'NONE', #5468, #5493 ) ;
#6660=DIRECTION ( 'NONE',  ( 0.000000000000000000, 1.000000000000000000, 0.000000000000000000 ) ) ;
#6665=MANIFOLD_SOLID_BREP ( 'Boss-Extrude1', #3227 ) ;
#6675=EDGE_LOOP ( 'NONE', ( #5556, #5529 ) ) ;
#6692=CARTESIAN_POINT ( 'NONE',  ( 0.000000000000000000, 0.2559055118110236116, 0.000000000000000000 ) ) ;
#6712=ORIENTED_EDGE ( 'NONE', *, *, #2292, .T. ) ;
#6726=DIRECTION ( 'NONE',  ( 0.000000000000000000, 0.000000000000000000, 1.000000000000000000 ) ) ;
#6728=SHAPE_DEFINITION_REPRESENTATION ( #3195, #1307 ) ;
#6794=EDGE_CURVE ( 'NONE', #997, #4290, #4157, .T. ) ;
#6820=ORIENTED_EDGE ( 'NONE', *, *, #2161, .F. ) ;
#6827=ADVANCED_FACE ( 'NONE', ( #7142, #3512, #4243 ), #4736, .F. ) ;
#6828=CARTESIAN_POINT ( 'NONE',  ( 0.000000000000000000, 0.000000000000000000, -0.2362204724409449341 ) ) ;
#6851=STYLED_ITEM('',(#7566),#6665);
#6930=PLANE ( 'NONE',  #4738 ) ;
#6984=FACE_OUTER_BOUND ( 'NONE', #4343, .T. ) ;
#7008=CIRCLE ( 'NONE', #2254, 0.2362204724409449341 ) ;
#7037=ORIENTED_EDGE ( 'NONE', *, *, #1018, .F. ) ;
#7062=VECTOR ( 'NONE', #7087, 39.37007874015748143 ) ;
#7065=FACE_BOUND ( 'NONE', #5458, .T. ) ;
#7070=VERTEX_POINT ( 'NONE', #3210 ) ;
#7087=DIRECTION ( 'NONE',  ( -0.000000000000000000, -1.000000000000000000, -0.000000000000000000 ) ) ;
#7099=CIRCLE ( 'NONE', #3811, 0.2362204724409455170 ) ;
#7142=FACE_OUTER_BOUND ( 'NONE', #3216, .T. ) ;
#7195=ORIENTED_EDGE ( 'NONE', *, *, #4259, .F. ) ;
#7238=DIRECTION ( 'NONE',  ( 0.000000000000000000, 1.000000000000000000, 0.000000000000000000 ) ) ;
#7240=DIRECTION ( 'NONE',  ( -1.000000000000000000, 0.000000000000000000, -0.000000000000000000 ) ) ;
#7304=CARTESIAN_POINT ( 'NONE',  ( 7.874015748031496287, 0.2559055118110236116, -0.4921259842519685179 ) ) ;
#7310=LENGTH_MEASURE_WITH_UNIT ( LENGTH_MEASURE( 0.02539999999999999897 ), #4414 );
#7317=CARTESIAN_POINT ( 'NONE',  ( 7.874015748031496287, 0.2559055118110236116, 0.000000000000000000 ) ) ;
#7334=ORIENTED_EDGE ( 'NONE', *, *, #2712, .F. ) ;
#7351=( NAMED_UNIT ( * ) PLANE_ANGLE_UNIT ( ) SI_UNIT ( $, .RADIAN. ) );
#7427=ADVANCED_FACE ( 'NONE', ( #3738 ), #306, .F. ) ;
#7473=VECTOR ( 'NONE', #3249, 39.37007874015748143 ) ;
#7497=DIMENSIONAL_EXPONENTS ( 1.000000000000000000, 0.000000000000000000, 0.000000000000000000, 0.000000000000000000, 0.000000000000000000, 0.000000000000000000, 0.000000000000000000 ) ;
#7560=COLOUR_RGB('Light Blue',0.38,0.62,0.78);
#7561=FILL_AREA_STYLE_COLOUR('',#7560);
#7562=FILL_AREA_STYLE('',(#7561));
#7563=SURFACE_STYLE_FILL_AREA(#7562);
#7564=SURFACE_SIDE_STYLE('',(#7563));
#7565=SURFACE_STYLE_USAGE(.BOTH.,#7564);
#7566=PRESENTATION_STYLE_ASSIGNMENT((#7565));
ENDSEC;
END-ISO-10303-21;
